ISO-10303-21;
HEADER;
FILE_DESCRIPTION (('STEP AP214'),
    '1' );
FILE_NAME ('O Ring Seal 2.step',
    '2026-10-05T22:38:29',
    ( '' ),
    ( '' ),
    'SwSTEP 2.0',
    'SolidWorks 2020',
    '' );
FILE_SCHEMA (( 'AUTOMOTIVE_DESIGN' ));
ENDSEC;

DATA;
#102=CARTESIAN_POINT ( 'NONE',  ( 20.10000000000000142, 11.84999999999999964, 0.000000000000000000 ) ) ;
#360=( LENGTH_UNIT ( ) NAMED_UNIT ( * ) SI_UNIT ( .MILLI., .METRE. ) );
#1079=CARTESIAN_POINT ( 'NONE',  ( 21.10000000000000142, 12.35000000006999876, 0.000000000000000000 ) ) ;
#1255=DIRECTION ( 'NONE',  ( -4.331025598861020273E-21, -3.276905820014099985E-06, 0.9999999999946310725 ) ) ;
#1273=DIRECTION ( 'NONE',  ( 0.000000000000000000, -1.000000000000000000, 0.000000000000000000 ) ) ;
#2046=DIRECTION ( 'NONE',  ( 0.000000000000000000, -1.000000000000000000, 0.000000000000000000 ) ) ;
#3736=CARTESIAN_POINT ( 'NONE',  ( 20.10000000000000142, 0.000000000000000000, 0.000000000000000000 ) ) ;
#3801=VERTEX_POINT ( 'NONE', #34713 ) ;
#3827=UNCERTAINTY_MEASURE_WITH_UNIT (LENGTH_MEASURE( 1.000000000000000082E-05 ), #61246, 'distance_accuracy_value', 'NONE');
#4075=DIRECTION ( 'NONE',  ( 1.000000000000000000, 0.000000000000000000, 0.000000000000000000 ) ) ;
#5748=VERTEX_POINT ( 'NONE', #28037 ) ;
#6820=CLOSED_SHELL ( 'NONE', ( #7260, #17489, #31796, #11532, #25813, #51411 ) ) ;
#7033=DIRECTION ( 'NONE',  ( 0.000000000000000000, -1.000000000000000000, 0.000000000000000000 ) ) ;
#7218=CARTESIAN_POINT ( 'NONE',  ( 21.10000000000000142, 0.000000000000000000, 0.000000000000000000 ) ) ;
#7260=ADVANCED_FACE ( 'NONE', ( #30449 ), #48360, .T. ) ;
#7328=( NAMED_UNIT ( * ) PLANE_ANGLE_UNIT ( ) SI_UNIT ( $, .RADIAN. ) );
#7665=ORIENTED_EDGE ( 'NONE', *, *, #56672, .F. ) ;
#8027=( NAMED_UNIT ( * ) SI_UNIT ( $, .STERADIAN. ) SOLID_ANGLE_UNIT ( ) );
#8079=MANIFOLD_SOLID_BREP ( 'Stock-MAS-678-1', #6820 ) ;
#8719=CARTESIAN_POINT ( 'NONE',  ( 20.10000000000000142, 12.35000000006999876, 0.000000000000000000 ) ) ;
#8764=ORIENTED_EDGE ( 'NONE', *, *, #42389, .F. ) ;
#9008=CIRCLE ( 'NONE', #48094, 12.35000000006999876 ) ;
#9312=CARTESIAN_POINT ( 'NONE',  ( 20.10000000000000142, -11.84999999999999964, 0.000000000000000000 ) ) ;
#9415=PRODUCT_DEFINITION_CONTEXT ( 'detailed design', #51657, 'design' ) ;
#9676=AXIS2_PLACEMENT_3D ( 'NONE', #40345, #19020, #18341 ) ;
#9799=ORIENTED_EDGE ( 'NONE', *, *, #20744, .T. ) ;
#9907=DIRECTION ( 'NONE',  ( 1.000000000000000000, 0.000000000000000000, 0.000000000000000000 ) ) ;
#10022=DIRECTION ( 'NONE',  ( -1.000000000000000000, 0.000000000000000000, 0.000000000000000000 ) ) ;
#11069=DIRECTION ( 'NONE',  ( -1.000000000000000000, 0.000000000000000000, 0.000000000000000000 ) ) ;
#11532=ADVANCED_FACE ( 'NONE', ( #26429 ), #36570, .F. ) ;
#11795=EDGE_LOOP ( 'NONE', ( #24072, #55179 ) ) ;
#12643=ORIENTED_EDGE ( 'NONE', *, *, #19486, .T. ) ;
#12931=FILL_AREA_STYLE_COLOUR ( '', #41035 ) ;
#13287=SHAPE_REPRESENTATION_RELATIONSHIP ( 'NONE' , 'NONE' ,  #60856, #42763 ) ;
#13501=CARTESIAN_POINT ( 'NONE',  ( 20.10000000000000142, 0.000000000000000000, 0.000000000000000000 ) ) ;
#13920=DIRECTION ( 'NONE',  ( 0.9999999999938153916, 3.516990153967770421E-06, 1.152484550329258267E-11 ) ) ;
#14365=STYLED_ITEM ( 'NONE', ( #33298 ), #8079 ) ;
#14511=TOROIDAL_SURFACE ( 'NONE', #56928, 12.35000000006999876, 0.5000000000000000000 ) ;
#15101=EDGE_CURVE ( 'NONE', #45349, #36624, #34384, .T. ) ;
#16993=CARTESIAN_POINT ( 'NONE',  ( 20.10000000000000142, 0.000000000000000000, 0.000000000000000000 ) ) ;
#17489=ADVANCED_FACE ( 'NONE', ( #61655 ), #14511, .T. ) ;
#17580=AXIS2_PLACEMENT_3D ( 'NONE', #65409, #18220, #7033 ) ;
#17705=COLOUR_RGB ( '', 0.72549020, 0.75294118, 0.79215686) ;
#18133=ORIENTED_EDGE ( 'NONE', *, *, #56625, .T. ) ;
#18220=DIRECTION ( 'NONE',  ( 1.000000000000000000, 0.000000000000000000, 0.000000000000000000 ) ) ;
#18268=ORIENTED_EDGE ( 'NONE', *, *, #35057, .T. ) ;
#18341=DIRECTION ( 'NONE',  ( 1.000000000000000000, 0.000000000000000000, 0.000000000000000000 ) ) ;
#19020=DIRECTION ( 'NONE',  ( 0.000000000000000000, 0.000000000000000000, 1.000000000000000000 ) ) ;
#19486=EDGE_CURVE ( 'NONE', #36624, #45349, #9008, .T. ) ;
#19561=CARTESIAN_POINT ( 'NONE',  ( 21.10000000000000142, -12.35000000006999876, 0.000000000000000000 ) ) ;
#20422=AXIS2_PLACEMENT_3D ( 'NONE', #3736, #10022, #41163 ) ;
#20702=FACE_OUTER_BOUND ( 'NONE', #33532, .T. ) ;
#20738=ORIENTED_EDGE ( 'NONE', *, *, #20744, .F. ) ;
#20744=EDGE_CURVE ( 'NONE', #55952, #58625, #31585, .T. ) ;
#21039=MECHANICAL_DESIGN_GEOMETRIC_PRESENTATION_REPRESENTATION('',(#14365),#44515);
#21619=DIRECTION ( 'NONE',  ( -1.000000000000000000, 0.000000000000000000, 0.000000000000000000 ) ) ;
#21879=DIRECTION ( 'NONE',  ( 0.9999999999938153916, -3.516990153967770421E-06, -1.152484550329258267E-11 ) ) ;
#21892=DIRECTION ( 'NONE',  ( 0.000000000000000000, 1.000000000000000000, 0.000000000000000000 ) ) ;
#22379=ORIENTED_EDGE ( 'NONE', *, *, #35057, .F. ) ;
#22900=ORIENTED_EDGE ( 'NONE', *, *, #58104, .F. ) ;
#22943=PLANE ( 'NONE',  #30572 ) ;
#23773=PRODUCT ( 'O Ring Seal 2', 'O Ring Seal 2', '', ( #41434 ) ) ;
#23819=AXIS2_PLACEMENT_3D ( 'NONE', #48806, #1255, #21879 ) ;
#24072=ORIENTED_EDGE ( 'NONE', *, *, #19486, .F. ) ;
#24630=VECTOR ( 'NONE', #9907, 1000.000000000000000 ) ;
#25510=UNCERTAINTY_MEASURE_WITH_UNIT (LENGTH_MEASURE( 1.000000000000000082E-05 ), #33563, 'distance_accuracy_value', 'NONE');
#25543=DIRECTION ( 'NONE',  ( 1.000000000000000000, 0.000000000000000000, 0.000000000000000000 ) ) ;
#25813=ADVANCED_FACE ( 'NONE', ( #20702 ), #42031, .F. ) ;
#26042=SHAPE_DEFINITION_REPRESENTATION ( #67327, #60856 ) ;
#26429=FACE_OUTER_BOUND ( 'NONE', #68119, .T. ) ;
#26827=ORIENTED_EDGE ( 'NONE', *, *, #56672, .T. ) ;
#27122=CIRCLE ( 'NONE', #20422, 11.84999999999999964 ) ;
#27221=CARTESIAN_POINT ( 'NONE',  ( 21.10000000000000142, 0.000000000000000000, 0.000000000000000000 ) ) ;
#27406=EDGE_CURVE ( 'NONE', #51112, #5748, #61737, .T. ) ;
#27717=CIRCLE ( 'NONE', #66784, 0.5000000000000014433 ) ;
#28037=CARTESIAN_POINT ( 'NONE',  ( 21.10000000000000142, -11.84999999999999964, 0.000000000000000000 ) ) ;
#28352=ORIENTED_EDGE ( 'NONE', *, *, #41458, .F. ) ;
#28476=PRODUCT_DEFINITION_FORMATION_WITH_SPECIFIED_SOURCE ( 'ANY', '', #23773, .NOT_KNOWN. ) ;
#28671=SURFACE_SIDE_STYLE ('',( #34611 ) ) ;
#28753=( NAMED_UNIT ( * ) PLANE_ANGLE_UNIT ( ) SI_UNIT ( $, .RADIAN. ) );
#29024=SURFACE_STYLE_USAGE ( .BOTH. , #28671 ) ;
#29100=( NAMED_UNIT ( * ) SI_UNIT ( $, .STERADIAN. ) SOLID_ANGLE_UNIT ( ) );
#29661=EDGE_LOOP ( 'NONE', ( #47488, #61259 ) ) ;
#30305=DIRECTION ( 'NONE',  ( 0.000000000000000000, -1.000000000000000000, 0.000000000000000000 ) ) ;
#30345=DIRECTION ( 'NONE',  ( -2.154007395656495261E-21, 3.276905819395100166E-06, -0.9999999999946310725 ) ) ;
#30449=FACE_OUTER_BOUND ( 'NONE', #38925, .T. ) ;
#30572=AXIS2_PLACEMENT_3D ( 'NONE', #7218, #66282, #34143 ) ;
#31585=LINE ( 'NONE', #102, #24630 ) ;
#31729=CIRCLE ( 'NONE', #64092, 11.84999999999999964 ) ;
#31796=ADVANCED_FACE ( 'NONE', ( #43593, #39379 ), #22943, .T. ) ;
#32030=AXIS2_PLACEMENT_3D ( 'NONE', #16993, #11069, #21892 ) ;
#32191=( NAMED_UNIT ( * ) SI_UNIT ( $, .STERADIAN. ) SOLID_ANGLE_UNIT ( ) );
#32470=ORIENTED_EDGE ( 'NONE', *, *, #27406, .T. ) ;
#32810=ORIENTED_EDGE ( 'NONE', *, *, #42921, .F. ) ;
#33255=STYLED_ITEM ( 'NONE', ( #55923 ), #42763 ) ;
#33298=PRESENTATION_STYLE_ASSIGNMENT (( #54961 ) ) ;
#33532=EDGE_LOOP ( 'NONE', ( #9799, #32810, #52532, #26827 ) ) ;
#33563=( LENGTH_UNIT ( ) NAMED_UNIT ( * ) SI_UNIT ( .MILLI., .METRE. ) );
#34134=CARTESIAN_POINT ( 'NONE',  ( 20.10000000000000142, 0.000000000000000000, 0.000000000000000000 ) ) ;
#34143=DIRECTION ( 'NONE',  ( 0.000000000000000000, 1.000000000000000000, 0.000000000000000000 ) ) ;
#34211=CARTESIAN_POINT ( 'NONE',  ( 21.10000000000000142, 0.000000000000000000, 0.000000000000000000 ) ) ;
#34384=CIRCLE ( 'NONE', #54427, 12.35000000006999876 ) ;
#34611=SURFACE_STYLE_FILL_AREA ( #54539 ) ;
#34713=CARTESIAN_POINT ( 'NONE',  ( 20.10000000000000142, -12.35000000006999876, 0.000000000000000000 ) ) ;
#35057=EDGE_CURVE ( 'NONE', #45349, #65308, #49514, .T. ) ;
#35581=AXIS2_PLACEMENT_3D ( 'NONE', #69070, #58580, #30305 ) ;
#36570=CYLINDRICAL_SURFACE ( 'NONE', #35581, 11.84999999999999964 ) ;
#36624=VERTEX_POINT ( 'NONE', #19561 ) ;
#37150=DIRECTION ( 'NONE',  ( 0.000000000000000000, 0.9999808993455937545, 0.006180691221632959691 ) ) ;
#37366=APPLICATION_CONTEXT ( 'automotive_design' ) ;
#38925=EDGE_LOOP ( 'NONE', ( #18268, #44017, #61538, #12643 ) ) ;
#39043=DIRECTION ( 'NONE',  ( 0.000000000000000000, 1.000000000000000000, 0.000000000000000000 ) ) ;
#39379=FACE_OUTER_BOUND ( 'NONE', #11795, .T. ) ;
#39844=VECTOR ( 'NONE', #62081, 1000.000000000000000 ) ;
#40345=CARTESIAN_POINT ( 'NONE',  ( 0.000000000000000000, 0.000000000000000000, 0.000000000000000000 ) ) ;
#40819=CARTESIAN_POINT ( 'NONE',  ( 20.60000000000000142, -12.34999999999999964, -4.046978686977000011E-05 ) ) ;
#41035=COLOUR_RGB ( '', 0.72549020, 0.75294118, 0.79215686) ;
#41163=DIRECTION ( 'NONE',  ( 0.000000000000000000, 1.000000000000000000, 0.000000000000000000 ) ) ;
#41434=PRODUCT_CONTEXT ( 'NONE', #37366, 'mechanical' ) ;
#41458=EDGE_CURVE ( 'NONE', #55952, #51112, #27122, .T. ) ;
#41965=ORIENTED_EDGE ( 'NONE', *, *, #15101, .T. ) ;
#42031=CYLINDRICAL_SURFACE ( 'NONE', #17580, 11.84999999999999964 ) ;
#42389=EDGE_CURVE ( 'NONE', #65308, #3801, #57707, .T. ) ;
#42668=( NAMED_UNIT ( * ) PLANE_ANGLE_UNIT ( ) SI_UNIT ( $, .RADIAN. ) );
#42763=ADVANCED_BREP_SHAPE_REPRESENTATION ( '', ( #8079, #9676 ), #57795 ) ;
#42921=EDGE_CURVE ( 'NONE', #5748, #58625, #46548, .T. ) ;
#43593=FACE_BOUND ( 'NONE', #29661, .T. ) ;
#43965=DIRECTION ( 'NONE',  ( -1.000000000000000000, 0.000000000000000000, 0.000000000000000000 ) ) ;
#44017=ORIENTED_EDGE ( 'NONE', *, *, #56625, .F. ) ;
#44254=ORIENTED_EDGE ( 'NONE', *, *, #42389, .T. ) ;
#44285=DIRECTION ( 'NONE',  ( -1.000000000000000000, 0.000000000000000000, 0.000000000000000000 ) ) ;
#44515=( GEOMETRIC_REPRESENTATION_CONTEXT ( 3 ) GLOBAL_UNCERTAINTY_ASSIGNED_CONTEXT ( ( #3827 ) ) GLOBAL_UNIT_ASSIGNED_CONTEXT ( ( #61246, #28753, #29100 ) ) REPRESENTATION_CONTEXT ( 'NONE', 'WORKASPACE' ) );
#44665=CARTESIAN_POINT ( 'NONE',  ( 21.10000000000000142, 0.000000000000000000, 0.000000000000000000 ) ) ;
#44979=DIRECTION ( 'NONE',  ( -1.000000000000000000, 0.000000000000000000, 0.000000000000000000 ) ) ;
#44988=CARTESIAN_POINT ( 'NONE',  ( 20.10000000000000142, -11.84999999999999964, 0.000000000000000000 ) ) ;
#45172=FILL_AREA_STYLE_COLOUR ( '', #17705 ) ;
#45349=VERTEX_POINT ( 'NONE', #1079 ) ;
#45443=AXIS2_PLACEMENT_3D ( 'NONE', #13501, #61037, #1273 ) ;
#45502=DIRECTION ( 'NONE',  ( 0.000000000000000000, -0.9999808993455937545, -0.006180691221632959691 ) ) ;
#45518=FILL_AREA_STYLE ('',( #45172 ) ) ;
#45920=CARTESIAN_POINT ( 'NONE',  ( 20.60000000000000142, 0.000000000000000000, 0.000000000000000000 ) ) ;
#46184=CARTESIAN_POINT ( 'NONE',  ( 20.60000000000000142, 0.000000000000000000, 0.000000000000000000 ) ) ;
#46401=FACE_OUTER_BOUND ( 'NONE', #69055, .T. ) ;
#46548=CIRCLE ( 'NONE', #55478, 11.84999999999999964 ) ;
#46636=AXIS2_PLACEMENT_3D ( 'NONE', #56889, #4075, #51297 ) ;
#47488=ORIENTED_EDGE ( 'NONE', *, *, #58104, .T. ) ;
#48094=AXIS2_PLACEMENT_3D ( 'NONE', #34211, #50282, #2046 ) ;
#48360=TOROIDAL_SURFACE ( 'NONE', #58443, 12.35000000006999876, 0.5000000000000000000 ) ;
#48806=CARTESIAN_POINT ( 'NONE',  ( 20.60000000000000142, 12.34999999999999964, 4.046978687741000012E-05 ) ) ;
#49514=CIRCLE ( 'NONE', #23819, 0.5000000000000014433 ) ;
#49540=DIRECTION ( 'NONE',  ( 0.000000000000000000, 1.000000000000000000, 0.000000000000000000 ) ) ;
#49624=PRODUCT_DEFINITION ( 'UNKNOWN', '', #28476, #9415 ) ;
#49971=( GEOMETRIC_REPRESENTATION_CONTEXT ( 3 ) GLOBAL_UNCERTAINTY_ASSIGNED_CONTEXT ( ( #25510 ) ) GLOBAL_UNIT_ASSIGNED_CONTEXT ( ( #33563, #7328, #8027 ) ) REPRESENTATION_CONTEXT ( 'NONE', 'WORKASPACE' ) );
#50282=DIRECTION ( 'NONE',  ( -1.000000000000000000, 0.000000000000000000, 0.000000000000000000 ) ) ;
#50547=DIRECTION ( 'NONE',  ( 0.000000000000000000, -1.000000000000000000, 0.000000000000000000 ) ) ;
#51112=VERTEX_POINT ( 'NONE', #9312 ) ;
#51297=DIRECTION ( 'NONE',  ( 0.000000000000000000, 1.000000000000000000, 0.000000000000000000 ) ) ;
#51411=ADVANCED_FACE ( 'NONE', ( #67025, #46401 ), #62126, .F. ) ;
#51657=APPLICATION_CONTEXT ( 'automotive_design' ) ;
#52532=ORIENTED_EDGE ( 'NONE', *, *, #27406, .F. ) ;
#52885=DIRECTION ( 'NONE',  ( 1.000000000000000000, 0.000000000000000000, 0.000000000000000000 ) ) ;
#52899=ORIENTED_EDGE ( 'NONE', *, *, #41458, .T. ) ;
#53100=DIRECTION ( 'NONE',  ( 0.000000000000000000, -1.000000000000000000, 0.000000000000000000 ) ) ;
#54427=AXIS2_PLACEMENT_3D ( 'NONE', #44665, #43965, #49540 ) ;
#54539=FILL_AREA_STYLE ('',( #12931 ) ) ;
#54961=SURFACE_STYLE_USAGE ( .BOTH. , #60899 ) ;
#55179=ORIENTED_EDGE ( 'NONE', *, *, #15101, .F. ) ;
#55309=SURFACE_STYLE_FILL_AREA ( #45518 ) ;
#55478=AXIS2_PLACEMENT_3D ( 'NONE', #27221, #21619, #53100 ) ;
#55567=MECHANICAL_DESIGN_GEOMETRIC_PRESENTATION_REPRESENTATION('',(#33255),#49971);
#55622=CARTESIAN_POINT ( 'NONE',  ( 20.10000000000000142, 11.84999999999999964, 0.000000000000000000 ) ) ;
#55923=PRESENTATION_STYLE_ASSIGNMENT (( #29024 ) ) ;
#55952=VERTEX_POINT ( 'NONE', #55622 ) ;
#56324=EDGE_CURVE ( 'NONE', #36624, #3801, #27717, .T. ) ;
#56615=CIRCLE ( 'NONE', #68880, 12.35000000006999876 ) ;
#56625=EDGE_CURVE ( 'NONE', #3801, #65308, #56615, .T. ) ;
#56672=EDGE_CURVE ( 'NONE', #51112, #55952, #57701, .T. ) ;
#56889=CARTESIAN_POINT ( 'NONE',  ( 20.10000000000000142, 0.000000000000000000, 0.000000000000000000 ) ) ;
#56928=AXIS2_PLACEMENT_3D ( 'NONE', #45920, #52885, #37150 ) ;
#57701=CIRCLE ( 'NONE', #45443, 11.84999999999999964 ) ;
#57707=CIRCLE ( 'NONE', #32030, 12.35000000006999876 ) ;
#57795=( GEOMETRIC_REPRESENTATION_CONTEXT ( 3 ) GLOBAL_UNCERTAINTY_ASSIGNED_CONTEXT ( ( #68835 ) ) GLOBAL_UNIT_ASSIGNED_CONTEXT ( ( #360, #42668, #32191 ) ) REPRESENTATION_CONTEXT ( 'NONE', 'WORKASPACE' ) );
#58104=EDGE_CURVE ( 'NONE', #58625, #5748, #31729, .T. ) ;
#58443=AXIS2_PLACEMENT_3D ( 'NONE', #46184, #25543, #45502 ) ;
#58580=DIRECTION ( 'NONE',  ( 1.000000000000000000, 0.000000000000000000, 0.000000000000000000 ) ) ;
#58625=VERTEX_POINT ( 'NONE', #59926 ) ;
#59926=CARTESIAN_POINT ( 'NONE',  ( 21.10000000000000142, 11.84999999999999964, 0.000000000000000000 ) ) ;
#60856=SHAPE_REPRESENTATION ( 'O Ring Seal 2', ( #9676 ), #57795 ) ;
#60899=SURFACE_SIDE_STYLE ('',( #55309 ) ) ;
#61037=DIRECTION ( 'NONE',  ( -1.000000000000000000, 0.000000000000000000, 0.000000000000000000 ) ) ;
#61246=( LENGTH_UNIT ( ) NAMED_UNIT ( * ) SI_UNIT ( .MILLI., .METRE. ) );
#61259=ORIENTED_EDGE ( 'NONE', *, *, #42921, .T. ) ;
#61538=ORIENTED_EDGE ( 'NONE', *, *, #56324, .F. ) ;
#61655=FACE_OUTER_BOUND ( 'NONE', #68107, .T. ) ;
#61737=LINE ( 'NONE', #44988, #39844 ) ;
#62081=DIRECTION ( 'NONE',  ( 1.000000000000000000, 0.000000000000000000, 0.000000000000000000 ) ) ;
#62126=PLANE ( 'NONE',  #46636 ) ;
#64092=AXIS2_PLACEMENT_3D ( 'NONE', #66972, #44979, #39043 ) ;
#64904=EDGE_LOOP ( 'NONE', ( #28352, #7665 ) ) ;
#65308=VERTEX_POINT ( 'NONE', #8719 ) ;
#65409=CARTESIAN_POINT ( 'NONE',  ( 20.10000000000000142, 0.000000000000000000, 0.000000000000000000 ) ) ;
#66282=DIRECTION ( 'NONE',  ( 1.000000000000000000, 0.000000000000000000, 0.000000000000000000 ) ) ;
#66784=AXIS2_PLACEMENT_3D ( 'NONE', #40819, #30345, #13920 ) ;
#66972=CARTESIAN_POINT ( 'NONE',  ( 21.10000000000000142, 0.000000000000000000, 0.000000000000000000 ) ) ;
#67025=FACE_BOUND ( 'NONE', #64904, .T. ) ;
#67327=PRODUCT_DEFINITION_SHAPE ( 'NONE', 'NONE',  #49624 ) ;
#67616=ORIENTED_EDGE ( 'NONE', *, *, #56324, .T. ) ;
#68107=EDGE_LOOP ( 'NONE', ( #67616, #8764, #22379, #41965 ) ) ;
#68119=EDGE_LOOP ( 'NONE', ( #32470, #22900, #20738, #52899 ) ) ;
#68835=UNCERTAINTY_MEASURE_WITH_UNIT (LENGTH_MEASURE( 1.000000000000000082E-05 ), #360, 'distance_accuracy_value', 'NONE');
#68880=AXIS2_PLACEMENT_3D ( 'NONE', #34134, #44285, #50547 ) ;
#69055=EDGE_LOOP ( 'NONE', ( #18133, #44254 ) ) ;
#69070=CARTESIAN_POINT ( 'NONE',  ( 20.10000000000000142, 0.000000000000000000, 0.000000000000000000 ) ) ;
ENDSEC;
END-ISO-10303-21;
